ISO-10303-21;
HEADER;
/* Generated by software containing ST-Developer
 * from STEP Tools, Inc. (www.steptools.com) 
 */

FILE_DESCRIPTION(
/* description */ ('Hinged panel with latch'),
/* implementation_level */ '2;1');

FILE_NAME(
/* name */ 'Hex Nut - M4.step',
/* time_stamp */ '2026-10-27T20:36:01-07:00',
/* author */ (''),
/* organization */ (''),
/* preprocessor_version */ 'ST-DEVELOPER v20.2',
/* originating_system */ 'Autodesk Translation Framework v15.17.0.0',
/* authorisation */ '');

FILE_SCHEMA (('AUTOMOTIVE_DESIGN { 1 0 10303 214 3 1 1 }'));
ENDSEC;

DATA;
#10=MECHANICAL_DESIGN_GEOMETRIC_PRESENTATION_REPRESENTATION('',(#307),#6743);
#207=(
BOUNDED_CURVE()
B_SPLINE_CURVE(2,(#6380,#6381,#6382),.UNSPECIFIED.,.F.,.F.)
B_SPLINE_CURVE_WITH_KNOTS((3,3),(0.137956735689167,0.609258407070138),
 .UNSPECIFIED.)
CURVE()
GEOMETRIC_REPRESENTATION_ITEM()
RATIONAL_B_SPLINE_CURVE((1.13260046146793,1.30781436262561,1.13260046146793))
REPRESENTATION_ITEM('')
);
#208=(
BOUNDED_CURVE()
B_SPLINE_CURVE(2,(#6384,#6385,#6386),.UNSPECIFIED.,.F.,.F.)
B_SPLINE_CURVE_WITH_KNOTS((3,3),(0.137956735689167,0.609258407070137),
 .UNSPECIFIED.)
CURVE()
GEOMETRIC_REPRESENTATION_ITEM()
RATIONAL_B_SPLINE_CURVE((1.13260046146793,1.30781436262561,1.13260046146793))
REPRESENTATION_ITEM('')
);
#209=(
BOUNDED_CURVE()
B_SPLINE_CURVE(2,(#6391,#6392,#6393),.UNSPECIFIED.,.F.,.F.)
B_SPLINE_CURVE_WITH_KNOTS((3,3),(0.137956735689167,0.609258407070138),
 .UNSPECIFIED.)
CURVE()
GEOMETRIC_REPRESENTATION_ITEM()
RATIONAL_B_SPLINE_CURVE((1.13260046146793,1.30781436262561,1.13260046146793))
REPRESENTATION_ITEM('')
);
#210=(
BOUNDED_CURVE()
B_SPLINE_CURVE(2,(#6395,#6396,#6397),.UNSPECIFIED.,.F.,.F.)
B_SPLINE_CURVE_WITH_KNOTS((3,3),(0.137956735689167,0.609258407070138),
 .UNSPECIFIED.)
CURVE()
GEOMETRIC_REPRESENTATION_ITEM()
RATIONAL_B_SPLINE_CURVE((1.13260046146793,1.30781436262561,1.13260046146793))
REPRESENTATION_ITEM('')
);
#211=(
BOUNDED_CURVE()
B_SPLINE_CURVE(2,(#6399,#6400,#6401),.UNSPECIFIED.,.F.,.F.)
B_SPLINE_CURVE_WITH_KNOTS((3,3),(0.137956735689167,0.609258407070138),
 .UNSPECIFIED.)
CURVE()
GEOMETRIC_REPRESENTATION_ITEM()
RATIONAL_B_SPLINE_CURVE((1.13260046146793,1.30781436262561,1.13260046146793))
REPRESENTATION_ITEM('')
);
#212=(
BOUNDED_CURVE()
B_SPLINE_CURVE(2,(#6402,#6403,#6404),.UNSPECIFIED.,.F.,.F.)
B_SPLINE_CURVE_WITH_KNOTS((3,3),(0.137956735689167,0.609258407070138),
 .UNSPECIFIED.)
CURVE()
GEOMETRIC_REPRESENTATION_ITEM()
RATIONAL_B_SPLINE_CURVE((1.13260046146793,1.30781436262561,1.13260046146793))
REPRESENTATION_ITEM('')
);
#213=(
BOUNDED_CURVE()
B_SPLINE_CURVE(2,(#6411,#6412,#6413),.UNSPECIFIED.,.F.,.F.)
B_SPLINE_CURVE_WITH_KNOTS((3,3),(0.137956735689167,0.609258407070138),
 .UNSPECIFIED.)
CURVE()
GEOMETRIC_REPRESENTATION_ITEM()
RATIONAL_B_SPLINE_CURVE((1.13260046146793,1.30781436262561,1.13260046146793))
REPRESENTATION_ITEM('')
);
#214=(
BOUNDED_CURVE()
B_SPLINE_CURVE(2,(#6415,#6416,#6417),.UNSPECIFIED.,.F.,.F.)
B_SPLINE_CURVE_WITH_KNOTS((3,3),(0.137956735689167,0.609258407070138),
 .UNSPECIFIED.)
CURVE()
GEOMETRIC_REPRESENTATION_ITEM()
RATIONAL_B_SPLINE_CURVE((1.13260046146793,1.30781436262561,1.13260046146793))
REPRESENTATION_ITEM('')
);
#215=(
BOUNDED_CURVE()
B_SPLINE_CURVE(2,(#6419,#6420,#6421),.UNSPECIFIED.,.F.,.F.)
B_SPLINE_CURVE_WITH_KNOTS((3,3),(0.137956735689167,0.609258407070138),
 .UNSPECIFIED.)
CURVE()
GEOMETRIC_REPRESENTATION_ITEM()
RATIONAL_B_SPLINE_CURVE((1.13260046146793,1.30781436262561,1.13260046146793))
REPRESENTATION_ITEM('')
);
#216=(
BOUNDED_CURVE()
B_SPLINE_CURVE(2,(#6423,#6424,#6425),.UNSPECIFIED.,.F.,.F.)
B_SPLINE_CURVE_WITH_KNOTS((3,3),(0.137956735689167,0.609258407070138),
 .UNSPECIFIED.)
CURVE()
GEOMETRIC_REPRESENTATION_ITEM()
RATIONAL_B_SPLINE_CURVE((1.13260046146793,1.30781436262561,1.13260046146793))
REPRESENTATION_ITEM('')
);
#217=(
BOUNDED_CURVE()
B_SPLINE_CURVE(2,(#6427,#6428,#6429),.UNSPECIFIED.,.F.,.F.)
B_SPLINE_CURVE_WITH_KNOTS((3,3),(0.137956735689167,0.609258407070138),
 .UNSPECIFIED.)
CURVE()
GEOMETRIC_REPRESENTATION_ITEM()
RATIONAL_B_SPLINE_CURVE((1.13260046146793,1.30781436262561,1.13260046146793))
REPRESENTATION_ITEM('')
);
#218=(
BOUNDED_CURVE()
B_SPLINE_CURVE(2,(#6430,#6431,#6432),.UNSPECIFIED.,.F.,.F.)
B_SPLINE_CURVE_WITH_KNOTS((3,3),(0.137956735689167,0.609258407070138),
 .UNSPECIFIED.)
CURVE()
GEOMETRIC_REPRESENTATION_ITEM()
RATIONAL_B_SPLINE_CURVE((1.13260046146793,1.30781436262561,1.13260046146793))
REPRESENTATION_ITEM('')
);
#249=CONICAL_SURFACE('',#4236,0.418322594216369,1.0471975511966);
#250=CONICAL_SURFACE('',#4238,0.418322594216369,1.0471975511966);
#275=SHAPE_REPRESENTATION_RELATIONSHIP('SRR','None',#6851,#291);
#291=ADVANCED_BREP_SHAPE_REPRESENTATION('',(#321),#6737);
#307=STYLED_ITEM('',(#7010),#321);
#321=MANIFOLD_SOLID_BREP('Body1',#3811);
#363=FACE_BOUND('',#932,.T.);
#364=FACE_BOUND('',#934,.T.);
#488=PLANE('',#4240);
#489=PLANE('',#4241);
#490=PLANE('',#4242);
#491=PLANE('',#4246);
#492=PLANE('',#4247);
#493=PLANE('',#4248);
#494=PLANE('',#4249);
#495=PLANE('',#4250);
#678=FACE_OUTER_BOUND('',#922,.T.);
#679=FACE_OUTER_BOUND('',#923,.T.);
#680=FACE_OUTER_BOUND('',#924,.T.);
#681=FACE_OUTER_BOUND('',#925,.T.);
#682=FACE_OUTER_BOUND('',#926,.T.);
#683=FACE_OUTER_BOUND('',#927,.T.);
#684=FACE_OUTER_BOUND('',#928,.T.);
#685=FACE_OUTER_BOUND('',#929,.T.);
#686=FACE_OUTER_BOUND('',#930,.T.);
#687=FACE_OUTER_BOUND('',#931,.T.);
#688=FACE_OUTER_BOUND('',#933,.T.);
#922=EDGE_LOOP('',(#3346,#3347,#3348,#3349,#3350,#3351,#3352,#3353,#3354));
#923=EDGE_LOOP('',(#3355,#3356,#3357,#3358,#3359,#3360,#3361,#3362,#3363));
#924=EDGE_LOOP('',(#3364,#3365,#3366,#3367));
#925=EDGE_LOOP('',(#3368,#3369,#3370,#3371));
#926=EDGE_LOOP('',(#3372,#3373,#3374,#3375));
#927=EDGE_LOOP('',(#3376,#3377,#3378,#3379));
#928=EDGE_LOOP('',(#3380,#3381,#3382,#3383));
#929=EDGE_LOOP('',(#3384,#3385,#3386,#3387));
#930=EDGE_LOOP('',(#3388,#3389,#3390,#3391));
#931=EDGE_LOOP('',(#3392));
#932=EDGE_LOOP('',(#3393));
#933=EDGE_LOOP('',(#3394));
#934=EDGE_LOOP('',(#3395));
#1282=LINE('',#6388,#1640);
#1283=LINE('',#6409,#1641);
#1284=LINE('',#6434,#1642);
#1285=LINE('',#6435,#1643);
#1286=LINE('',#6437,#1644);
#1287=LINE('',#6439,#1645);
#1288=LINE('',#6444,#1646);
#1289=LINE('',#6447,#1647);
#1290=LINE('',#6449,#1648);
#1640=VECTOR('',#5150,0.418322594216369);
#1641=VECTOR('',#5157,0.418322594216369);
#1642=VECTOR('',#5160,1.);
#1643=VECTOR('',#5161,1.);
#1644=VECTOR('',#5164,1.);
#1645=VECTOR('',#5167,1.);
#1646=VECTOR('',#5172,0.2);
#1647=VECTOR('',#5177,1.);
#1648=VECTOR('',#5180,1.);
#1768=CIRCLE('',#4237,0.3325);
#1769=CIRCLE('',#4239,0.3325);
#1770=CIRCLE('',#4244,0.1666);
#1771=CIRCLE('',#4245,0.1666);
#2040=VERTEX_POINT('',#6378);
#2041=VERTEX_POINT('',#6379);
#2042=VERTEX_POINT('',#6383);
#2043=VERTEX_POINT('',#6387);
#2044=VERTEX_POINT('',#6390);
#2045=VERTEX_POINT('',#6394);
#2046=VERTEX_POINT('',#6398);
#2047=VERTEX_POINT('',#6406);
#2048=VERTEX_POINT('',#6408);
#2049=VERTEX_POINT('',#6410);
#2050=VERTEX_POINT('',#6414);
#2051=VERTEX_POINT('',#6418);
#2052=VERTEX_POINT('',#6422);
#2053=VERTEX_POINT('',#6426);
#2054=VERTEX_POINT('',#6441);
#2055=VERTEX_POINT('',#6443);
#2485=EDGE_CURVE('',#2040,#2041,#207,.T.);
#2486=EDGE_CURVE('',#2042,#2040,#208,.T.);
#2487=EDGE_CURVE('',#2042,#2043,#1282,.T.);
#2488=EDGE_CURVE('',#2043,#2043,#1768,.T.);
#2489=EDGE_CURVE('',#2044,#2042,#209,.T.);
#2490=EDGE_CURVE('',#2045,#2044,#210,.T.);
#2491=EDGE_CURVE('',#2046,#2045,#211,.T.);
#2492=EDGE_CURVE('',#2041,#2046,#212,.T.);
#2493=EDGE_CURVE('',#2047,#2047,#1769,.T.);
#2494=EDGE_CURVE('',#2047,#2048,#1283,.T.);
#2495=EDGE_CURVE('',#2049,#2048,#213,.T.);
#2496=EDGE_CURVE('',#2050,#2049,#214,.T.);
#2497=EDGE_CURVE('',#2051,#2050,#215,.T.);
#2498=EDGE_CURVE('',#2052,#2051,#216,.T.);
#2499=EDGE_CURVE('',#2053,#2052,#217,.T.);
#2500=EDGE_CURVE('',#2048,#2053,#218,.T.);
#2501=EDGE_CURVE('',#2044,#2053,#1284,.T.);
#2502=EDGE_CURVE('',#2045,#2052,#1285,.T.);
#2503=EDGE_CURVE('',#2042,#2048,#1286,.T.);
#2504=EDGE_CURVE('',#2040,#2049,#1287,.T.);
#2505=EDGE_CURVE('',#2054,#2054,#1770,.F.);
#2506=EDGE_CURVE('',#2054,#2055,#1288,.T.);
#2507=EDGE_CURVE('',#2055,#2055,#1771,.F.);
#2508=EDGE_CURVE('',#2041,#2050,#1289,.T.);
#2509=EDGE_CURVE('',#2046,#2051,#1290,.T.);
#3346=ORIENTED_EDGE('',*,*,#2485,.F.);
#3347=ORIENTED_EDGE('',*,*,#2486,.F.);
#3348=ORIENTED_EDGE('',*,*,#2487,.T.);
#3349=ORIENTED_EDGE('',*,*,#2488,.F.);
#3350=ORIENTED_EDGE('',*,*,#2487,.F.);
#3351=ORIENTED_EDGE('',*,*,#2489,.F.);
#3352=ORIENTED_EDGE('',*,*,#2490,.F.);
#3353=ORIENTED_EDGE('',*,*,#2491,.F.);
#3354=ORIENTED_EDGE('',*,*,#2492,.F.);
#3355=ORIENTED_EDGE('',*,*,#2493,.F.);
#3356=ORIENTED_EDGE('',*,*,#2494,.T.);
#3357=ORIENTED_EDGE('',*,*,#2495,.F.);
#3358=ORIENTED_EDGE('',*,*,#2496,.F.);
#3359=ORIENTED_EDGE('',*,*,#2497,.F.);
#3360=ORIENTED_EDGE('',*,*,#2498,.F.);
#3361=ORIENTED_EDGE('',*,*,#2499,.F.);
#3362=ORIENTED_EDGE('',*,*,#2500,.F.);
#3363=ORIENTED_EDGE('',*,*,#2494,.F.);
#3364=ORIENTED_EDGE('',*,*,#2490,.T.);
#3365=ORIENTED_EDGE('',*,*,#2501,.T.);
#3366=ORIENTED_EDGE('',*,*,#2499,.T.);
#3367=ORIENTED_EDGE('',*,*,#2502,.F.);
#3368=ORIENTED_EDGE('',*,*,#2489,.T.);
#3369=ORIENTED_EDGE('',*,*,#2503,.T.);
#3370=ORIENTED_EDGE('',*,*,#2500,.T.);
#3371=ORIENTED_EDGE('',*,*,#2501,.F.);
#3372=ORIENTED_EDGE('',*,*,#2486,.T.);
#3373=ORIENTED_EDGE('',*,*,#2504,.T.);
#3374=ORIENTED_EDGE('',*,*,#2495,.T.);
#3375=ORIENTED_EDGE('',*,*,#2503,.F.);
#3376=ORIENTED_EDGE('',*,*,#2505,.F.);
#3377=ORIENTED_EDGE('',*,*,#2506,.T.);
#3378=ORIENTED_EDGE('',*,*,#2507,.T.);
#3379=ORIENTED_EDGE('',*,*,#2506,.F.);
#3380=ORIENTED_EDGE('',*,*,#2485,.T.);
#3381=ORIENTED_EDGE('',*,*,#2508,.T.);
#3382=ORIENTED_EDGE('',*,*,#2496,.T.);
#3383=ORIENTED_EDGE('',*,*,#2504,.F.);
#3384=ORIENTED_EDGE('',*,*,#2491,.T.);
#3385=ORIENTED_EDGE('',*,*,#2502,.T.);
#3386=ORIENTED_EDGE('',*,*,#2498,.T.);
#3387=ORIENTED_EDGE('',*,*,#2509,.F.);
#3388=ORIENTED_EDGE('',*,*,#2492,.T.);
#3389=ORIENTED_EDGE('',*,*,#2509,.T.);
#3390=ORIENTED_EDGE('',*,*,#2497,.T.);
#3391=ORIENTED_EDGE('',*,*,#2508,.F.);
#3392=ORIENTED_EDGE('',*,*,#2493,.T.);
#3393=ORIENTED_EDGE('',*,*,#2505,.T.);
#3394=ORIENTED_EDGE('',*,*,#2488,.T.);
#3395=ORIENTED_EDGE('',*,*,#2507,.F.);
#3585=CYLINDRICAL_SURFACE('',#4243,0.1666);
#3747=ADVANCED_FACE('',(#678),#249,.T.);
#3748=ADVANCED_FACE('',(#679),#250,.T.);
#3749=ADVANCED_FACE('',(#680),#488,.T.);
#3750=ADVANCED_FACE('',(#681),#489,.T.);
#3751=ADVANCED_FACE('',(#682),#490,.T.);
#3752=ADVANCED_FACE('',(#683),#3585,.F.);
#3753=ADVANCED_FACE('',(#684),#491,.T.);
#3754=ADVANCED_FACE('',(#685),#492,.T.);
#3755=ADVANCED_FACE('',(#686),#493,.T.);
#3756=ADVANCED_FACE('',(#687,#363),#494,.T.);
#3757=ADVANCED_FACE('',(#688,#364),#495,.F.);
#3811=CLOSED_SHELL('',(#3747,#3748,#3749,#3750,#3751,#3752,#3753,#3754,
#3755,#3756,#3757));
#4235=AXIS2_PLACEMENT_3D('',#6376,#5146,#5147);
#4236=AXIS2_PLACEMENT_3D('',#6377,#5148,#5149);
#4237=AXIS2_PLACEMENT_3D('',#6389,#5151,#5152);
#4238=AXIS2_PLACEMENT_3D('',#6405,#5153,#5154);
#4239=AXIS2_PLACEMENT_3D('',#6407,#5155,#5156);
#4240=AXIS2_PLACEMENT_3D('',#6433,#5158,#5159);
#4241=AXIS2_PLACEMENT_3D('',#6436,#5162,#5163);
#4242=AXIS2_PLACEMENT_3D('',#6438,#5165,#5166);
#4243=AXIS2_PLACEMENT_3D('',#6440,#5168,#5169);
#4244=AXIS2_PLACEMENT_3D('',#6442,#5170,#5171);
#4245=AXIS2_PLACEMENT_3D('',#6445,#5173,#5174);
#4246=AXIS2_PLACEMENT_3D('',#6446,#5175,#5176);
#4247=AXIS2_PLACEMENT_3D('',#6448,#5178,#5179);
#4248=AXIS2_PLACEMENT_3D('',#6450,#5181,#5182);
#4249=AXIS2_PLACEMENT_3D('',#6451,#5183,#5184);
#4250=AXIS2_PLACEMENT_3D('',#6452,#5185,#5186);
#5146=DIRECTION('axis',(0.,0.,1.));
#5147=DIRECTION('refdir',(1.,0.,0.));
#5148=DIRECTION('center_axis',(0.,1.,0.));
#5149=DIRECTION('ref_axis',(1.,0.,0.));
#5150=DIRECTION('',(0.866025403784439,-0.5,1.06057523872491E-16));
#5151=DIRECTION('center_axis',(0.,-1.,0.));
#5152=DIRECTION('ref_axis',(1.,0.,0.));
#5153=DIRECTION('center_axis',(0.,-1.,0.));
#5154=DIRECTION('ref_axis',(1.,0.,0.));
#5155=DIRECTION('center_axis',(0.,1.,0.));
#5156=DIRECTION('ref_axis',(1.,0.,0.));
#5157=DIRECTION('',(-0.866025403784439,-0.5,-1.06057523872491E-16));
#5158=DIRECTION('center_axis',(1.37354477598826E-16,0.,-1.));
#5159=DIRECTION('ref_axis',(-1.,0.,-1.37354477598826E-16));
#5160=DIRECTION('',(0.,1.,0.));
#5161=DIRECTION('',(0.,1.,0.));
#5162=DIRECTION('center_axis',(-0.866025403784439,0.,-0.5));
#5163=DIRECTION('ref_axis',(-0.5,0.,0.866025403784439));
#5164=DIRECTION('',(0.,1.,0.));
#5165=DIRECTION('center_axis',(-0.866025403784439,0.,0.5));
#5166=DIRECTION('ref_axis',(0.5,0.,0.866025403784439));
#5167=DIRECTION('',(0.,1.,0.));
#5168=DIRECTION('center_axis',(0.,1.,0.));
#5169=DIRECTION('ref_axis',(1.,0.,0.));
#5170=DIRECTION('center_axis',(0.,1.,0.));
#5171=DIRECTION('ref_axis',(1.,0.,0.));
#5172=DIRECTION('',(0.,-1.,0.));
#5173=DIRECTION('center_axis',(0.,1.,0.));
#5174=DIRECTION('ref_axis',(1.,0.,0.));
#5175=DIRECTION('center_axis',(-1.37354477598826E-16,0.,1.));
#5176=DIRECTION('ref_axis',(1.,0.,1.37354477598826E-16));
#5177=DIRECTION('',(0.,1.,0.));
#5178=DIRECTION('center_axis',(0.866025403784439,0.,-0.5));
#5179=DIRECTION('ref_axis',(-0.5,0.,-0.866025403784439));
#5180=DIRECTION('',(0.,1.,0.));
#5181=DIRECTION('center_axis',(0.866025403784439,0.,0.5));
#5182=DIRECTION('ref_axis',(0.5,0.,-0.866025403784439));
#5183=DIRECTION('center_axis',(0.,1.,0.));
#5184=DIRECTION('ref_axis',(1.,0.,0.));
#5185=DIRECTION('center_axis',(0.,1.,0.));
#5186=DIRECTION('ref_axis',(1.,0.,0.));
#6376=CARTESIAN_POINT('',(0.,0.,0.));
#6377=CARTESIAN_POINT('Origin',(0.,0.0495496978733727,0.));
#6378=CARTESIAN_POINT('',(-0.202072594216369,0.0413643688277828,0.35));
#6379=CARTESIAN_POINT('',(0.202072594216369,0.0413643688277828,0.35));
#6380=CARTESIAN_POINT('Ctrl Pts',(-0.202072594216369,0.0413643688277828,
0.35));
#6381=CARTESIAN_POINT('Ctrl Pts',(-1.66533453693773E-16,-0.0169689645055507,
0.35));
#6382=CARTESIAN_POINT('Ctrl Pts',(0.202072594216369,0.0413643688277828,
0.35));
#6383=CARTESIAN_POINT('',(-0.404145188432738,0.0413643688277828,-4.94935111404956E-17));
#6384=CARTESIAN_POINT('Ctrl Pts',(-0.404145188432738,0.0413643688277828,
-4.94935111404956E-17));
#6385=CARTESIAN_POINT('Ctrl Pts',(-0.303108891324553,-0.0169689645055504,
0.175));
#6386=CARTESIAN_POINT('Ctrl Pts',(-0.202072594216369,0.0413643688277828,
0.35));
#6387=CARTESIAN_POINT('',(-0.3325,0.,-4.07195060716495E-17));
#6388=CARTESIAN_POINT('',(-0.418322594216369,0.0495496978733727,-5.12297426018093E-17));
#6389=CARTESIAN_POINT('Origin',(0.,0.,0.));
#6390=CARTESIAN_POINT('',(-0.202072594216369,0.0413643688277828,-0.35));
#6391=CARTESIAN_POINT('Ctrl Pts',(-0.202072594216369,0.0413643688277828,
-0.35));
#6392=CARTESIAN_POINT('Ctrl Pts',(-0.303108891324553,-0.0169689645055505,
-0.175));
#6393=CARTESIAN_POINT('Ctrl Pts',(-0.404145188432738,0.0413643688277828,
-4.94935111404956E-17));
#6394=CARTESIAN_POINT('',(0.202072594216369,0.0413643688277828,-0.35));
#6395=CARTESIAN_POINT('Ctrl Pts',(0.202072594216369,0.0413643688277828,
-0.35));
#6396=CARTESIAN_POINT('Ctrl Pts',(-2.77555756156289E-17,-0.0169689645055504,
-0.35));
#6397=CARTESIAN_POINT('Ctrl Pts',(-0.202072594216369,0.0413643688277828,
-0.35));
#6398=CARTESIAN_POINT('',(0.404145188432738,0.0413643688277828,0.));
#6399=CARTESIAN_POINT('Ctrl Pts',(0.404145188432738,0.0413643688277828,
0.));
#6400=CARTESIAN_POINT('Ctrl Pts',(0.303108891324553,-0.0169689645055505,
-0.175));
#6401=CARTESIAN_POINT('Ctrl Pts',(0.202072594216369,0.0413643688277828,
-0.35));
#6402=CARTESIAN_POINT('Ctrl Pts',(0.202072594216369,0.0413643688277828,
0.35));
#6403=CARTESIAN_POINT('Ctrl Pts',(0.303108891324554,-0.0169689645055505,
0.175));
#6404=CARTESIAN_POINT('Ctrl Pts',(0.404145188432738,0.0413643688277828,
0.));
#6405=CARTESIAN_POINT('Origin',(0.,0.270450302126627,0.));
#6406=CARTESIAN_POINT('',(-0.3325,0.32,-4.07195060716495E-17));
#6407=CARTESIAN_POINT('Origin',(0.,0.32,0.));
#6408=CARTESIAN_POINT('',(-0.404145188432738,0.278635631172217,-4.94935111404957E-17));
#6409=CARTESIAN_POINT('',(-0.418322594216369,0.270450302126627,-5.12297426018093E-17));
#6410=CARTESIAN_POINT('',(-0.202072594216369,0.278635631172217,0.35));
#6411=CARTESIAN_POINT('Ctrl Pts',(-0.202072594216369,0.278635631172217,
0.35));
#6412=CARTESIAN_POINT('Ctrl Pts',(-0.303108891324554,0.33696896450555,0.175));
#6413=CARTESIAN_POINT('Ctrl Pts',(-0.404145188432738,0.278635631172217,
-4.94935111404957E-17));
#6414=CARTESIAN_POINT('',(0.202072594216369,0.278635631172217,0.35));
#6415=CARTESIAN_POINT('Ctrl Pts',(0.202072594216369,0.278635631172217,0.35));
#6416=CARTESIAN_POINT('Ctrl Pts',(-1.38777878078145E-16,0.336968964505551,
0.35));
#6417=CARTESIAN_POINT('Ctrl Pts',(-0.202072594216369,0.278635631172217,
0.35));
#6418=CARTESIAN_POINT('',(0.404145188432738,0.278635631172217,0.));
#6419=CARTESIAN_POINT('Ctrl Pts',(0.404145188432738,0.278635631172217,0.));
#6420=CARTESIAN_POINT('Ctrl Pts',(0.303108891324553,0.336968964505551,0.175));
#6421=CARTESIAN_POINT('Ctrl Pts',(0.202072594216369,0.278635631172217,0.35));
#6422=CARTESIAN_POINT('',(0.202072594216369,0.278635631172217,-0.35));
#6423=CARTESIAN_POINT('Ctrl Pts',(0.202072594216369,0.278635631172217,-0.35));
#6424=CARTESIAN_POINT('Ctrl Pts',(0.303108891324554,0.336968964505551,-0.175));
#6425=CARTESIAN_POINT('Ctrl Pts',(0.404145188432738,0.278635631172217,0.));
#6426=CARTESIAN_POINT('',(-0.202072594216369,0.278635631172217,-0.35));
#6427=CARTESIAN_POINT('Ctrl Pts',(-0.202072594216369,0.278635631172217,
-0.35));
#6428=CARTESIAN_POINT('Ctrl Pts',(8.32667268468867E-17,0.33696896450555,
-0.35));
#6429=CARTESIAN_POINT('Ctrl Pts',(0.202072594216369,0.278635631172217,-0.35));
#6430=CARTESIAN_POINT('Ctrl Pts',(-0.404145188432738,0.278635631172217,
-4.94935111404957E-17));
#6431=CARTESIAN_POINT('Ctrl Pts',(-0.303108891324553,0.33696896450555,-0.175));
#6432=CARTESIAN_POINT('Ctrl Pts',(-0.202072594216369,0.278635631172217,
-0.35));
#6433=CARTESIAN_POINT('Origin',(0.202072594216369,0.,-0.35));
#6434=CARTESIAN_POINT('',(-0.202072594216369,0.,-0.35));
#6435=CARTESIAN_POINT('',(0.202072594216369,0.,-0.35));
#6436=CARTESIAN_POINT('Origin',(-0.202072594216369,0.,-0.35));
#6437=CARTESIAN_POINT('',(-0.404145188432738,0.,-4.94935111404957E-17));
#6438=CARTESIAN_POINT('Origin',(-0.404145188432738,0.,-4.94935111404957E-17));
#6439=CARTESIAN_POINT('',(-0.202072594216369,0.,0.35));
#6440=CARTESIAN_POINT('Origin',(0.,0.,0.));
#6441=CARTESIAN_POINT('',(-0.1666,0.32,2.04026156737949E-17));
#6442=CARTESIAN_POINT('Origin',(0.,0.32,0.));
#6443=CARTESIAN_POINT('',(-0.1666,0.,2.04026156737949E-17));
#6444=CARTESIAN_POINT('',(-0.1666,0.,2.04026156737949E-17));
#6445=CARTESIAN_POINT('Origin',(0.,0.,0.));
#6446=CARTESIAN_POINT('Origin',(-0.202072594216369,0.,0.35));
#6447=CARTESIAN_POINT('',(0.202072594216369,0.,0.35));
#6448=CARTESIAN_POINT('Origin',(0.404145188432738,0.,0.));
#6449=CARTESIAN_POINT('',(0.404145188432738,0.,0.));
#6450=CARTESIAN_POINT('Origin',(0.202072594216369,0.,0.35));
#6451=CARTESIAN_POINT('Origin',(0.,0.32,0.));
#6452=CARTESIAN_POINT('Origin',(0.,0.,0.));
#6716=UNCERTAINTY_MEASURE_WITH_UNIT(LENGTH_MEASURE(0.001),#6744,
'DISTANCE_ACCURACY_VALUE',
'Maximum model space distance between geometric entities at asserted c
onnectivities');
#6722=UNCERTAINTY_MEASURE_WITH_UNIT(LENGTH_MEASURE(0.001),#6744,
'DISTANCE_ACCURACY_VALUE',
'Maximum model space distance between geometric entities at asserted c
onnectivities');
#6737=(
GEOMETRIC_REPRESENTATION_CONTEXT(3)
GLOBAL_UNCERTAINTY_ASSIGNED_CONTEXT((#6716))
GLOBAL_UNIT_ASSIGNED_CONTEXT((#6744,#6746,#6747))
REPRESENTATION_CONTEXT('','3D')
);
#6743=(
GEOMETRIC_REPRESENTATION_CONTEXT(3)
GLOBAL_UNCERTAINTY_ASSIGNED_CONTEXT((#6722))
GLOBAL_UNIT_ASSIGNED_CONTEXT((#6744,#6746,#6747))
REPRESENTATION_CONTEXT('','3D')
);
#6744=(
LENGTH_UNIT()
NAMED_UNIT(*)
SI_UNIT(.CENTI.,.METRE.)
);
#6746=(
NAMED_UNIT(*)
PLANE_ANGLE_UNIT()
SI_UNIT($,.RADIAN.)
);
#6747=(
NAMED_UNIT(*)
SI_UNIT($,.STERADIAN.)
SOLID_ANGLE_UNIT()
);
#6762=SHAPE_DEFINITION_REPRESENTATION(#6782,#6851);
#6782=PRODUCT_DEFINITION_SHAPE('',$,#6872);
#6851=SHAPE_REPRESENTATION('',(#4235),#6737);
#6857=PRODUCT_DEFINITION_CONTEXT('part definition',#6919,'design');
#6872=PRODUCT_DEFINITION('Hex Nut - M4','Hex Nut - M4',#6892,#6857);
#6892=PRODUCT_DEFINITION_FORMATION('',$,#6935);
#6919=APPLICATION_CONTEXT(
'Core Data for Automotive Mechanical Design Process');
#6920=PRODUCT_CONTEXT('part definition',#6919,'mechanical');
#6935=PRODUCT('Hex Nut - M4','Hex Nut - M4','Hex Nut - M4',(#6920));
#7004=COLOUR_RGB('Black',0.12,0.14,0.17);
#7005=FILL_AREA_STYLE_COLOUR('',#7004);
#7006=FILL_AREA_STYLE('',(#7005));
#7007=SURFACE_STYLE_FILL_AREA(#7006);
#7008=SURFACE_SIDE_STYLE('',(#7007));
#7009=SURFACE_STYLE_USAGE(.BOTH.,#7008);
#7010=PRESENTATION_STYLE_ASSIGNMENT((#7009));
ENDSEC;
END-ISO-10303-21;
